ISO-10303-21;
HEADER;
/* Generated by software containing ST-Developer
 * from STEP Tools, Inc. (www.steptools.com) 
 */

FILE_DESCRIPTION(
/* description */ (''),
/* implementation_level */ '2;1');

FILE_NAME(
/* name */ 'Guide_Rail_02.step',
/* time_stamp */ '2026-10-19T02:00:06+06:00',
/* author */ (''),
/* organization */ (''),
/* preprocessor_version */ 'ST-DEVELOPER v20.2',
/* originating_system */ 'Autodesk Translation Framework v15.15.0.0',
/* authorisation */ '');

FILE_SCHEMA (('AUTOMOTIVE_DESIGN { 1 0 10303 214 3 1 1 }'));
ENDSEC;

DATA;
#10=MECHANICAL_DESIGN_GEOMETRIC_PRESENTATION_REPRESENTATION('',(#106),#4833);
#84=SHAPE_REPRESENTATION_RELATIONSHIP('SRR','None',#4875,#95);
#95=ADVANCED_BREP_SHAPE_REPRESENTATION('',(#117),#4823);
#106=STYLED_ITEM('',(#5006),#117);
#117=MANIFOLD_SOLID_BREP('Guide_Rail_02',#2688);
#133=FACE_BOUND('',#470,.T.);
#134=FACE_BOUND('',#471,.T.);
#135=FACE_BOUND('',#472,.T.);
#136=FACE_BOUND('',#473,.T.);
#137=FACE_BOUND('',#474,.T.);
#138=FACE_BOUND('',#475,.T.);
#176=PLANE('',#2856);
#177=PLANE('',#2860);
#178=PLANE('',#2864);
#179=PLANE('',#2868);
#180=PLANE('',#2872);
#181=PLANE('',#2876);
#182=PLANE('',#2877);
#183=PLANE('',#2878);
#184=PLANE('',#2879);
#185=PLANE('',#2880);
#186=PLANE('',#2881);
#187=PLANE('',#2882);
#286=FACE_OUTER_BOUND('',#453,.T.);
#287=FACE_OUTER_BOUND('',#454,.T.);
#288=FACE_OUTER_BOUND('',#455,.T.);
#289=FACE_OUTER_BOUND('',#456,.T.);
#290=FACE_OUTER_BOUND('',#457,.T.);
#291=FACE_OUTER_BOUND('',#458,.T.);
#292=FACE_OUTER_BOUND('',#459,.T.);
#293=FACE_OUTER_BOUND('',#460,.T.);
#294=FACE_OUTER_BOUND('',#461,.T.);
#295=FACE_OUTER_BOUND('',#462,.T.);
#296=FACE_OUTER_BOUND('',#463,.T.);
#297=FACE_OUTER_BOUND('',#464,.T.);
#298=FACE_OUTER_BOUND('',#465,.T.);
#299=FACE_OUTER_BOUND('',#466,.T.);
#300=FACE_OUTER_BOUND('',#467,.T.);
#301=FACE_OUTER_BOUND('',#468,.T.);
#302=FACE_OUTER_BOUND('',#469,.T.);
#303=FACE_OUTER_BOUND('',#476,.T.);
#453=EDGE_LOOP('',(#1837,#1838,#1839,#1840));
#454=EDGE_LOOP('',(#1841));
#455=EDGE_LOOP('',(#1842,#1843,#1844,#1845));
#456=EDGE_LOOP('',(#1846));
#457=EDGE_LOOP('',(#1847,#1848,#1849,#1850));
#458=EDGE_LOOP('',(#1851));
#459=EDGE_LOOP('',(#1852,#1853,#1854,#1855));
#460=EDGE_LOOP('',(#1856));
#461=EDGE_LOOP('',(#1857,#1858,#1859,#1860));
#462=EDGE_LOOP('',(#1861));
#463=EDGE_LOOP('',(#1862,#1863,#1864,#1865));
#464=EDGE_LOOP('',(#1866));
#465=EDGE_LOOP('',(#1867,#1868,#1869,#1870));
#466=EDGE_LOOP('',(#1871,#1872,#1873,#1874));
#467=EDGE_LOOP('',(#1875,#1876,#1877,#1878));
#468=EDGE_LOOP('',(#1879,#1880,#1881,#1882));
#469=EDGE_LOOP('',(#1883,#1884,#1885,#1886));
#470=EDGE_LOOP('',(#1887));
#471=EDGE_LOOP('',(#1888));
#472=EDGE_LOOP('',(#1889));
#473=EDGE_LOOP('',(#1890));
#474=EDGE_LOOP('',(#1891));
#475=EDGE_LOOP('',(#1892));
#476=EDGE_LOOP('',(#1893,#1894,#1895,#1896));
#645=LINE('',#3959,#899);
#646=LINE('',#3966,#900);
#647=LINE('',#3973,#901);
#648=LINE('',#3980,#902);
#649=LINE('',#3987,#903);
#650=LINE('',#3994,#904);
#651=LINE('',#4000,#905);
#652=LINE('',#4002,#906);
#653=LINE('',#4004,#907);
#654=LINE('',#4005,#908);
#655=LINE('',#4008,#909);
#656=LINE('',#4010,#910);
#657=LINE('',#4011,#911);
#658=LINE('',#4014,#912);
#659=LINE('',#4016,#913);
#660=LINE('',#4017,#914);
#661=LINE('',#4019,#915);
#662=LINE('',#4020,#916);
#899=VECTOR('',#3178,4.);
#900=VECTOR('',#3187,4.);
#901=VECTOR('',#3196,4.);
#902=VECTOR('',#3205,4.);
#903=VECTOR('',#3214,4.);
#904=VECTOR('',#3223,4.);
#905=VECTOR('',#3230,10.);
#906=VECTOR('',#3231,10.);
#907=VECTOR('',#3232,10.);
#908=VECTOR('',#3233,10.);
#909=VECTOR('',#3236,10.);
#910=VECTOR('',#3237,10.);
#911=VECTOR('',#3238,10.);
#912=VECTOR('',#3241,10.);
#913=VECTOR('',#3242,10.);
#914=VECTOR('',#3243,10.);
#915=VECTOR('',#3246,10.);
#916=VECTOR('',#3247,10.);
#1147=CIRCLE('',#2854,4.);
#1148=CIRCLE('',#2855,4.);
#1149=CIRCLE('',#2858,4.);
#1150=CIRCLE('',#2859,4.);
#1151=CIRCLE('',#2862,4.);
#1152=CIRCLE('',#2863,4.);
#1153=CIRCLE('',#2866,4.);
#1154=CIRCLE('',#2867,4.);
#1155=CIRCLE('',#2870,4.);
#1156=CIRCLE('',#2871,4.);
#1157=CIRCLE('',#2874,4.);
#1158=CIRCLE('',#2875,4.);
#1225=VERTEX_POINT('',#3956);
#1226=VERTEX_POINT('',#3958);
#1227=VERTEX_POINT('',#3963);
#1228=VERTEX_POINT('',#3965);
#1229=VERTEX_POINT('',#3970);
#1230=VERTEX_POINT('',#3972);
#1231=VERTEX_POINT('',#3977);
#1232=VERTEX_POINT('',#3979);
#1233=VERTEX_POINT('',#3984);
#1234=VERTEX_POINT('',#3986);
#1235=VERTEX_POINT('',#3991);
#1236=VERTEX_POINT('',#3993);
#1237=VERTEX_POINT('',#3998);
#1238=VERTEX_POINT('',#3999);
#1239=VERTEX_POINT('',#4001);
#1240=VERTEX_POINT('',#4003);
#1241=VERTEX_POINT('',#4007);
#1242=VERTEX_POINT('',#4009);
#1243=VERTEX_POINT('',#4013);
#1244=VERTEX_POINT('',#4015);
#1459=EDGE_CURVE('',#1225,#1225,#1147,.T.);
#1460=EDGE_CURVE('',#1225,#1226,#645,.T.);
#1461=EDGE_CURVE('',#1226,#1226,#1148,.T.);
#1462=EDGE_CURVE('',#1227,#1227,#1149,.T.);
#1463=EDGE_CURVE('',#1227,#1228,#646,.T.);
#1464=EDGE_CURVE('',#1228,#1228,#1150,.T.);
#1465=EDGE_CURVE('',#1229,#1229,#1151,.T.);
#1466=EDGE_CURVE('',#1229,#1230,#647,.T.);
#1467=EDGE_CURVE('',#1230,#1230,#1152,.T.);
#1468=EDGE_CURVE('',#1231,#1231,#1153,.T.);
#1469=EDGE_CURVE('',#1231,#1232,#648,.T.);
#1470=EDGE_CURVE('',#1232,#1232,#1154,.T.);
#1471=EDGE_CURVE('',#1233,#1233,#1155,.T.);
#1472=EDGE_CURVE('',#1233,#1234,#649,.T.);
#1473=EDGE_CURVE('',#1234,#1234,#1156,.T.);
#1474=EDGE_CURVE('',#1235,#1235,#1157,.T.);
#1475=EDGE_CURVE('',#1235,#1236,#650,.T.);
#1476=EDGE_CURVE('',#1236,#1236,#1158,.T.);
#1477=EDGE_CURVE('',#1237,#1238,#651,.T.);
#1478=EDGE_CURVE('',#1237,#1239,#652,.T.);
#1479=EDGE_CURVE('',#1240,#1239,#653,.T.);
#1480=EDGE_CURVE('',#1238,#1240,#654,.T.);
#1481=EDGE_CURVE('',#1238,#1241,#655,.T.);
#1482=EDGE_CURVE('',#1242,#1240,#656,.T.);
#1483=EDGE_CURVE('',#1241,#1242,#657,.T.);
#1484=EDGE_CURVE('',#1241,#1243,#658,.T.);
#1485=EDGE_CURVE('',#1244,#1242,#659,.T.);
#1486=EDGE_CURVE('',#1243,#1244,#660,.T.);
#1487=EDGE_CURVE('',#1243,#1237,#661,.T.);
#1488=EDGE_CURVE('',#1239,#1244,#662,.T.);
#1837=ORIENTED_EDGE('',*,*,#1459,.F.);
#1838=ORIENTED_EDGE('',*,*,#1460,.T.);
#1839=ORIENTED_EDGE('',*,*,#1461,.T.);
#1840=ORIENTED_EDGE('',*,*,#1460,.F.);
#1841=ORIENTED_EDGE('',*,*,#1461,.F.);
#1842=ORIENTED_EDGE('',*,*,#1462,.F.);
#1843=ORIENTED_EDGE('',*,*,#1463,.T.);
#1844=ORIENTED_EDGE('',*,*,#1464,.T.);
#1845=ORIENTED_EDGE('',*,*,#1463,.F.);
#1846=ORIENTED_EDGE('',*,*,#1464,.F.);
#1847=ORIENTED_EDGE('',*,*,#1465,.F.);
#1848=ORIENTED_EDGE('',*,*,#1466,.T.);
#1849=ORIENTED_EDGE('',*,*,#1467,.T.);
#1850=ORIENTED_EDGE('',*,*,#1466,.F.);
#1851=ORIENTED_EDGE('',*,*,#1467,.F.);
#1852=ORIENTED_EDGE('',*,*,#1468,.F.);
#1853=ORIENTED_EDGE('',*,*,#1469,.T.);
#1854=ORIENTED_EDGE('',*,*,#1470,.T.);
#1855=ORIENTED_EDGE('',*,*,#1469,.F.);
#1856=ORIENTED_EDGE('',*,*,#1470,.F.);
#1857=ORIENTED_EDGE('',*,*,#1471,.F.);
#1858=ORIENTED_EDGE('',*,*,#1472,.T.);
#1859=ORIENTED_EDGE('',*,*,#1473,.T.);
#1860=ORIENTED_EDGE('',*,*,#1472,.F.);
#1861=ORIENTED_EDGE('',*,*,#1473,.F.);
#1862=ORIENTED_EDGE('',*,*,#1474,.F.);
#1863=ORIENTED_EDGE('',*,*,#1475,.T.);
#1864=ORIENTED_EDGE('',*,*,#1476,.T.);
#1865=ORIENTED_EDGE('',*,*,#1475,.F.);
#1866=ORIENTED_EDGE('',*,*,#1476,.F.);
#1867=ORIENTED_EDGE('',*,*,#1477,.F.);
#1868=ORIENTED_EDGE('',*,*,#1478,.T.);
#1869=ORIENTED_EDGE('',*,*,#1479,.F.);
#1870=ORIENTED_EDGE('',*,*,#1480,.F.);
#1871=ORIENTED_EDGE('',*,*,#1481,.F.);
#1872=ORIENTED_EDGE('',*,*,#1480,.T.);
#1873=ORIENTED_EDGE('',*,*,#1482,.F.);
#1874=ORIENTED_EDGE('',*,*,#1483,.F.);
#1875=ORIENTED_EDGE('',*,*,#1484,.F.);
#1876=ORIENTED_EDGE('',*,*,#1483,.T.);
#1877=ORIENTED_EDGE('',*,*,#1485,.F.);
#1878=ORIENTED_EDGE('',*,*,#1486,.F.);
#1879=ORIENTED_EDGE('',*,*,#1487,.F.);
#1880=ORIENTED_EDGE('',*,*,#1486,.T.);
#1881=ORIENTED_EDGE('',*,*,#1488,.F.);
#1882=ORIENTED_EDGE('',*,*,#1478,.F.);
#1883=ORIENTED_EDGE('',*,*,#1488,.T.);
#1884=ORIENTED_EDGE('',*,*,#1485,.T.);
#1885=ORIENTED_EDGE('',*,*,#1482,.T.);
#1886=ORIENTED_EDGE('',*,*,#1479,.T.);
#1887=ORIENTED_EDGE('',*,*,#1474,.T.);
#1888=ORIENTED_EDGE('',*,*,#1471,.T.);
#1889=ORIENTED_EDGE('',*,*,#1468,.T.);
#1890=ORIENTED_EDGE('',*,*,#1465,.T.);
#1891=ORIENTED_EDGE('',*,*,#1462,.T.);
#1892=ORIENTED_EDGE('',*,*,#1459,.T.);
#1893=ORIENTED_EDGE('',*,*,#1487,.T.);
#1894=ORIENTED_EDGE('',*,*,#1477,.T.);
#1895=ORIENTED_EDGE('',*,*,#1481,.T.);
#1896=ORIENTED_EDGE('',*,*,#1484,.T.);
#2479=CYLINDRICAL_SURFACE('',#2853,4.);
#2480=CYLINDRICAL_SURFACE('',#2857,4.);
#2481=CYLINDRICAL_SURFACE('',#2861,4.);
#2482=CYLINDRICAL_SURFACE('',#2865,4.);
#2483=CYLINDRICAL_SURFACE('',#2869,4.);
#2484=CYLINDRICAL_SURFACE('',#2873,4.);
#2544=ADVANCED_FACE('',(#286),#2479,.F.);
#2545=ADVANCED_FACE('',(#287),#176,.T.);
#2546=ADVANCED_FACE('',(#288),#2480,.F.);
#2547=ADVANCED_FACE('',(#289),#177,.T.);
#2548=ADVANCED_FACE('',(#290),#2481,.F.);
#2549=ADVANCED_FACE('',(#291),#178,.T.);
#2550=ADVANCED_FACE('',(#292),#2482,.F.);
#2551=ADVANCED_FACE('',(#293),#179,.T.);
#2552=ADVANCED_FACE('',(#294),#2483,.F.);
#2553=ADVANCED_FACE('',(#295),#180,.T.);
#2554=ADVANCED_FACE('',(#296),#2484,.F.);
#2555=ADVANCED_FACE('',(#297),#181,.T.);
#2556=ADVANCED_FACE('',(#298),#182,.T.);
#2557=ADVANCED_FACE('',(#299),#183,.T.);
#2558=ADVANCED_FACE('',(#300),#184,.T.);
#2559=ADVANCED_FACE('',(#301),#185,.T.);
#2560=ADVANCED_FACE('',(#302,#133,#134,#135,#136,#137,#138),#186,.T.);
#2561=ADVANCED_FACE('',(#303),#187,.F.);
#2688=CLOSED_SHELL('',(#2544,#2545,#2546,#2547,#2548,#2549,#2550,#2551,
#2552,#2553,#2554,#2555,#2556,#2557,#2558,#2559,#2560,#2561));
#2852=AXIS2_PLACEMENT_3D('',#3954,#3172,#3173);
#2853=AXIS2_PLACEMENT_3D('',#3955,#3174,#3175);
#2854=AXIS2_PLACEMENT_3D('',#3957,#3176,#3177);
#2855=AXIS2_PLACEMENT_3D('',#3960,#3179,#3180);
#2856=AXIS2_PLACEMENT_3D('',#3961,#3181,#3182);
#2857=AXIS2_PLACEMENT_3D('',#3962,#3183,#3184);
#2858=AXIS2_PLACEMENT_3D('',#3964,#3185,#3186);
#2859=AXIS2_PLACEMENT_3D('',#3967,#3188,#3189);
#2860=AXIS2_PLACEMENT_3D('',#3968,#3190,#3191);
#2861=AXIS2_PLACEMENT_3D('',#3969,#3192,#3193);
#2862=AXIS2_PLACEMENT_3D('',#3971,#3194,#3195);
#2863=AXIS2_PLACEMENT_3D('',#3974,#3197,#3198);
#2864=AXIS2_PLACEMENT_3D('',#3975,#3199,#3200);
#2865=AXIS2_PLACEMENT_3D('',#3976,#3201,#3202);
#2866=AXIS2_PLACEMENT_3D('',#3978,#3203,#3204);
#2867=AXIS2_PLACEMENT_3D('',#3981,#3206,#3207);
#2868=AXIS2_PLACEMENT_3D('',#3982,#3208,#3209);
#2869=AXIS2_PLACEMENT_3D('',#3983,#3210,#3211);
#2870=AXIS2_PLACEMENT_3D('',#3985,#3212,#3213);
#2871=AXIS2_PLACEMENT_3D('',#3988,#3215,#3216);
#2872=AXIS2_PLACEMENT_3D('',#3989,#3217,#3218);
#2873=AXIS2_PLACEMENT_3D('',#3990,#3219,#3220);
#2874=AXIS2_PLACEMENT_3D('',#3992,#3221,#3222);
#2875=AXIS2_PLACEMENT_3D('',#3995,#3224,#3225);
#2876=AXIS2_PLACEMENT_3D('',#3996,#3226,#3227);
#2877=AXIS2_PLACEMENT_3D('',#3997,#3228,#3229);
#2878=AXIS2_PLACEMENT_3D('',#4006,#3234,#3235);
#2879=AXIS2_PLACEMENT_3D('',#4012,#3239,#3240);
#2880=AXIS2_PLACEMENT_3D('',#4018,#3244,#3245);
#2881=AXIS2_PLACEMENT_3D('',#4021,#3248,#3249);
#2882=AXIS2_PLACEMENT_3D('',#4022,#3250,#3251);
#3172=DIRECTION('axis',(0.,0.,1.));
#3173=DIRECTION('refdir',(1.,0.,0.));
#3174=DIRECTION('center_axis',(0.,0.,-1.));
#3175=DIRECTION('ref_axis',(-1.,0.,0.));
#3176=DIRECTION('center_axis',(0.,0.,-1.));
#3177=DIRECTION('ref_axis',(-1.,0.,0.));
#3178=DIRECTION('',(0.,0.,-1.));
#3179=DIRECTION('center_axis',(0.,0.,-1.));
#3180=DIRECTION('ref_axis',(-1.,0.,0.));
#3181=DIRECTION('center_axis',(0.,0.,1.));
#3182=DIRECTION('ref_axis',(-1.,0.,0.));
#3183=DIRECTION('center_axis',(0.,0.,-1.));
#3184=DIRECTION('ref_axis',(-1.,0.,0.));
#3185=DIRECTION('center_axis',(0.,0.,-1.));
#3186=DIRECTION('ref_axis',(-1.,0.,0.));
#3187=DIRECTION('',(0.,0.,-1.));
#3188=DIRECTION('center_axis',(0.,0.,-1.));
#3189=DIRECTION('ref_axis',(-1.,0.,0.));
#3190=DIRECTION('center_axis',(0.,0.,1.));
#3191=DIRECTION('ref_axis',(-1.,0.,0.));
#3192=DIRECTION('center_axis',(0.,0.,-1.));
#3193=DIRECTION('ref_axis',(-1.,0.,0.));
#3194=DIRECTION('center_axis',(0.,0.,-1.));
#3195=DIRECTION('ref_axis',(-1.,0.,0.));
#3196=DIRECTION('',(0.,0.,-1.));
#3197=DIRECTION('center_axis',(0.,0.,-1.));
#3198=DIRECTION('ref_axis',(-1.,0.,0.));
#3199=DIRECTION('center_axis',(0.,0.,1.));
#3200=DIRECTION('ref_axis',(-1.,0.,0.));
#3201=DIRECTION('center_axis',(0.,0.,-1.));
#3202=DIRECTION('ref_axis',(-1.,0.,0.));
#3203=DIRECTION('center_axis',(0.,0.,-1.));
#3204=DIRECTION('ref_axis',(-1.,0.,0.));
#3205=DIRECTION('',(0.,0.,-1.));
#3206=DIRECTION('center_axis',(0.,0.,-1.));
#3207=DIRECTION('ref_axis',(-1.,0.,0.));
#3208=DIRECTION('center_axis',(0.,0.,1.));
#3209=DIRECTION('ref_axis',(-1.,0.,0.));
#3210=DIRECTION('center_axis',(0.,0.,-1.));
#3211=DIRECTION('ref_axis',(-1.,0.,0.));
#3212=DIRECTION('center_axis',(0.,0.,-1.));
#3213=DIRECTION('ref_axis',(-1.,0.,0.));
#3214=DIRECTION('',(0.,0.,-1.));
#3215=DIRECTION('center_axis',(0.,0.,-1.));
#3216=DIRECTION('ref_axis',(-1.,0.,0.));
#3217=DIRECTION('center_axis',(0.,0.,1.));
#3218=DIRECTION('ref_axis',(-1.,0.,0.));
#3219=DIRECTION('center_axis',(0.,0.,-1.));
#3220=DIRECTION('ref_axis',(-1.,0.,0.));
#3221=DIRECTION('center_axis',(0.,0.,-1.));
#3222=DIRECTION('ref_axis',(-1.,0.,0.));
#3223=DIRECTION('',(0.,0.,-1.));
#3224=DIRECTION('center_axis',(0.,0.,-1.));
#3225=DIRECTION('ref_axis',(-1.,0.,0.));
#3226=DIRECTION('center_axis',(0.,0.,1.));
#3227=DIRECTION('ref_axis',(-1.,0.,0.));
#3228=DIRECTION('center_axis',(1.,0.,0.));
#3229=DIRECTION('ref_axis',(0.,1.,0.));
#3230=DIRECTION('',(0.,-1.,0.));
#3231=DIRECTION('',(0.,0.,1.));
#3232=DIRECTION('',(0.,1.,0.));
#3233=DIRECTION('',(0.,0.,1.));
#3234=DIRECTION('center_axis',(0.,-1.,0.));
#3235=DIRECTION('ref_axis',(1.,0.,0.));
#3236=DIRECTION('',(-1.,0.,0.));
#3237=DIRECTION('',(1.,0.,0.));
#3238=DIRECTION('',(0.,0.,1.));
#3239=DIRECTION('center_axis',(-1.,0.,0.));
#3240=DIRECTION('ref_axis',(0.,-1.,0.));
#3241=DIRECTION('',(0.,1.,0.));
#3242=DIRECTION('',(0.,-1.,0.));
#3243=DIRECTION('',(0.,0.,1.));
#3244=DIRECTION('center_axis',(0.,1.,0.));
#3245=DIRECTION('ref_axis',(-1.,0.,0.));
#3246=DIRECTION('',(1.,0.,0.));
#3247=DIRECTION('',(-1.,0.,0.));
#3248=DIRECTION('center_axis',(0.,0.,1.));
#3249=DIRECTION('ref_axis',(1.,0.,0.));
#3250=DIRECTION('center_axis',(0.,0.,1.));
#3251=DIRECTION('ref_axis',(-1.,0.,0.));
#3954=CARTESIAN_POINT('',(0.,0.,0.));
#3955=CARTESIAN_POINT('Origin',(56.,14.9999999999895,14.0000000000021));
#3956=CARTESIAN_POINT('',(60.,14.9999999999895,14.0000000000021));
#3957=CARTESIAN_POINT('Origin',(56.,14.9999999999895,14.0000000000021));
#3958=CARTESIAN_POINT('',(60.,14.9999999999895,8.00000000000211));
#3959=CARTESIAN_POINT('',(60.,14.9999999999895,14.0000000000021));
#3960=CARTESIAN_POINT('Origin',(56.,14.9999999999895,8.00000000000211));
#3961=CARTESIAN_POINT('Origin',(56.,14.9999999999895,8.00000000000211));
#3962=CARTESIAN_POINT('Origin',(-48.,14.9999999999895,14.0000000000021));
#3963=CARTESIAN_POINT('',(-44.,14.9999999999895,14.0000000000021));
#3964=CARTESIAN_POINT('Origin',(-48.,14.9999999999895,14.0000000000021));
#3965=CARTESIAN_POINT('',(-44.,14.9999999999895,8.00000000000211));
#3966=CARTESIAN_POINT('',(-44.,14.9999999999895,14.0000000000021));
#3967=CARTESIAN_POINT('Origin',(-48.,14.9999999999895,8.00000000000211));
#3968=CARTESIAN_POINT('Origin',(-48.,14.9999999999895,8.00000000000211));
#3969=CARTESIAN_POINT('Origin',(-22.,14.9999999999895,14.0000000000021));
#3970=CARTESIAN_POINT('',(-18.,14.9999999999895,14.0000000000021));
#3971=CARTESIAN_POINT('Origin',(-22.,14.9999999999895,14.0000000000021));
#3972=CARTESIAN_POINT('',(-18.,14.9999999999895,8.00000000000211));
#3973=CARTESIAN_POINT('',(-18.,14.9999999999895,14.0000000000021));
#3974=CARTESIAN_POINT('Origin',(-22.,14.9999999999895,8.00000000000211));
#3975=CARTESIAN_POINT('Origin',(-22.,14.9999999999895,8.00000000000211));
#3976=CARTESIAN_POINT('Origin',(30.,14.9999999999895,14.0000000000021));
#3977=CARTESIAN_POINT('',(34.,14.9999999999895,14.0000000000021));
#3978=CARTESIAN_POINT('Origin',(30.,14.9999999999895,14.0000000000021));
#3979=CARTESIAN_POINT('',(34.,14.9999999999895,8.00000000000211));
#3980=CARTESIAN_POINT('',(34.,14.9999999999895,14.0000000000021));
#3981=CARTESIAN_POINT('Origin',(30.,14.9999999999895,8.00000000000211));
#3982=CARTESIAN_POINT('Origin',(30.,14.9999999999895,8.00000000000211));
#3983=CARTESIAN_POINT('Origin',(-74.,14.9999999999895,14.0000000000021));
#3984=CARTESIAN_POINT('',(-70.,14.9999999999895,14.0000000000021));
#3985=CARTESIAN_POINT('Origin',(-74.,14.9999999999895,14.0000000000021));
#3986=CARTESIAN_POINT('',(-70.,14.9999999999895,8.00000000000211));
#3987=CARTESIAN_POINT('',(-70.,14.9999999999895,14.0000000000021));
#3988=CARTESIAN_POINT('Origin',(-74.,14.9999999999895,8.00000000000211));
#3989=CARTESIAN_POINT('Origin',(-74.,14.9999999999895,8.00000000000211));
#3990=CARTESIAN_POINT('Origin',(4.,14.9999999999895,14.0000000000021));
#3991=CARTESIAN_POINT('',(8.,14.9999999999895,14.0000000000021));
#3992=CARTESIAN_POINT('Origin',(4.,14.9999999999895,14.0000000000021));
#3993=CARTESIAN_POINT('',(8.,14.9999999999895,8.00000000000211));
#3994=CARTESIAN_POINT('',(8.,14.9999999999895,14.0000000000021));
#3995=CARTESIAN_POINT('Origin',(4.,14.9999999999895,8.00000000000211));
#3996=CARTESIAN_POINT('Origin',(4.,14.9999999999895,8.00000000000211));
#3997=CARTESIAN_POINT('Origin',(70.,8.99999999998948,4.00000000000212));
#3998=CARTESIAN_POINT('',(70.,20.9999999999895,4.00000000000212));
#3999=CARTESIAN_POINT('',(70.,8.99999999998948,4.00000000000212));
#4000=CARTESIAN_POINT('',(70.,20.9999999999895,4.00000000000212));
#4001=CARTESIAN_POINT('',(70.,20.9999999999895,14.0000000000021));
#4002=CARTESIAN_POINT('',(70.,20.9999999999895,4.00000000000212));
#4003=CARTESIAN_POINT('',(70.,8.99999999998948,14.0000000000021));
#4004=CARTESIAN_POINT('',(70.,20.9999999999895,14.0000000000021));
#4005=CARTESIAN_POINT('',(70.,8.99999999998948,4.00000000000212));
#4006=CARTESIAN_POINT('Origin',(-90.,8.99999999998948,4.00000000000212));
#4007=CARTESIAN_POINT('',(-90.,8.99999999998948,4.00000000000212));
#4008=CARTESIAN_POINT('',(70.,8.99999999998948,4.00000000000212));
#4009=CARTESIAN_POINT('',(-90.,8.99999999998948,14.0000000000021));
#4010=CARTESIAN_POINT('',(70.,8.99999999998948,14.0000000000021));
#4011=CARTESIAN_POINT('',(-90.,8.99999999998948,4.00000000000212));
#4012=CARTESIAN_POINT('Origin',(-90.,20.9999999999895,4.00000000000212));
#4013=CARTESIAN_POINT('',(-90.,20.9999999999895,4.00000000000212));
#4014=CARTESIAN_POINT('',(-90.,8.99999999998948,4.00000000000212));
#4015=CARTESIAN_POINT('',(-90.,20.9999999999895,14.0000000000021));
#4016=CARTESIAN_POINT('',(-90.,8.99999999998948,14.0000000000021));
#4017=CARTESIAN_POINT('',(-90.,20.9999999999895,4.00000000000212));
#4018=CARTESIAN_POINT('Origin',(70.,20.9999999999895,4.00000000000212));
#4019=CARTESIAN_POINT('',(-90.,20.9999999999895,4.00000000000212));
#4020=CARTESIAN_POINT('',(-90.,20.9999999999895,14.0000000000021));
#4021=CARTESIAN_POINT('Origin',(-10.,14.9999999999895,14.0000000000021));
#4022=CARTESIAN_POINT('Origin',(-10.,14.9999999999895,4.00000000000212));
#4810=UNCERTAINTY_MEASURE_WITH_UNIT(LENGTH_MEASURE(0.01),#4834,
'DISTANCE_ACCURACY_VALUE',
'Maximum model space distance between geometric entities at asserted c
onnectivities');
#4820=UNCERTAINTY_MEASURE_WITH_UNIT(LENGTH_MEASURE(0.01),#4834,
'DISTANCE_ACCURACY_VALUE',
'Maximum model space distance between geometric entities at asserted c
onnectivities');
#4823=(
GEOMETRIC_REPRESENTATION_CONTEXT(3)
GLOBAL_UNCERTAINTY_ASSIGNED_CONTEXT((#4810))
GLOBAL_UNIT_ASSIGNED_CONTEXT((#4834,#4836,#4837))
REPRESENTATION_CONTEXT('','3D')
);
#4833=(
GEOMETRIC_REPRESENTATION_CONTEXT(3)
GLOBAL_UNCERTAINTY_ASSIGNED_CONTEXT((#4820))
GLOBAL_UNIT_ASSIGNED_CONTEXT((#4834,#4836,#4837))
REPRESENTATION_CONTEXT('','3D')
);
#4834=(
LENGTH_UNIT()
NAMED_UNIT(*)
SI_UNIT(.MILLI.,.METRE.)
);
#4836=(
NAMED_UNIT(*)
PLANE_ANGLE_UNIT()
SI_UNIT($,.RADIAN.)
);
#4837=(
NAMED_UNIT(*)
SI_UNIT($,.STERADIAN.)
SOLID_ANGLE_UNIT()
);
#4840=SHAPE_DEFINITION_REPRESENTATION(#4852,#4875);
#4852=PRODUCT_DEFINITION_SHAPE('',$,#4888);
#4875=SHAPE_REPRESENTATION('',(#2852),#4823);
#4885=PRODUCT_DEFINITION_CONTEXT('part definition',#4923,'design');
#4888=PRODUCT_DEFINITION('Guide_Rail_02','Guide_Rail_02',#4900,#4885);
#4900=PRODUCT_DEFINITION_FORMATION('',$,#4927);
#4923=APPLICATION_CONTEXT(
'Core Data for Automotive Mechanical Design Process');
#4924=PRODUCT_CONTEXT('part definition',#4923,'mechanical');
#4927=PRODUCT('Guide_Rail_02','Guide_Rail_02',$,(#4924));
#5000=COLOUR_RGB('Off White',0.89,0.88,0.83);
#5001=FILL_AREA_STYLE_COLOUR('',#5000);
#5002=FILL_AREA_STYLE('',(#5001));
#5003=SURFACE_STYLE_FILL_AREA(#5002);
#5004=SURFACE_SIDE_STYLE('',(#5003));
#5005=SURFACE_STYLE_USAGE(.BOTH.,#5004);
#5006=PRESENTATION_STYLE_ASSIGNMENT((#5005));
ENDSEC;
END-ISO-10303-21;
